ISO-10303-21;
HEADER;
/* Generated by software containing ST-Developer
 * from STEP Tools, Inc. (www.steptools.com) 
 */

FILE_DESCRIPTION(
/* description */ ('PAT-099'),
/* implementation_level */ '2;1');

FILE_NAME(
/* name */ 'M5x14 Cap Screw.step',
/* time_stamp */ '2026-10-29T17:25:42-07:00',
/* author */ (''),
/* organization */ (''),
/* preprocessor_version */ 'ST-DEVELOPER v20.2',
/* originating_system */ 'Autodesk Translation Framework v15.17.0.0',
/* authorisation */ '');

FILE_SCHEMA (('AUTOMOTIVE_DESIGN { 1 0 10303 214 3 1 1 }'));
ENDSEC;

DATA;
#10=MECHANICAL_DESIGN_GEOMETRIC_PRESENTATION_REPRESENTATION('',(#346),#11035);
#29=CONICAL_SURFACE('',#5324,0.4,0.785398163397448);
#30=CONICAL_SURFACE('',#5328,0.41,0.785398163397448);
#31=CONICAL_SURFACE('',#5332,0.26,0.463647609000806);
#40=ORIENTED_CLOSED_SHELL('',*,#4714,.F.);
#42=BREP_WITH_VOIDS('Body1',#4715,(#40));
#296=SHAPE_REPRESENTATION_RELATIONSHIP('SRR','None',#11165,#321);
#321=ADVANCED_BREP_SHAPE_REPRESENTATION('',(#42),#11015);
#346=STYLED_ITEM('',(#11393),#42);
#489=FACE_BOUND('',#1172,.T.);
#579=PLANE('',#5312);
#580=PLANE('',#5313);
#581=PLANE('',#5314);
#582=PLANE('',#5315);
#583=PLANE('',#5316);
#584=PLANE('',#5317);
#585=PLANE('',#5318);
#586=PLANE('',#5319);
#587=PLANE('',#5320);
#588=PLANE('',#5322);
#589=PLANE('',#5330);
#789=FACE_OUTER_BOUND('',#1158,.T.);
#790=FACE_OUTER_BOUND('',#1159,.T.);
#791=FACE_OUTER_BOUND('',#1160,.T.);
#792=FACE_OUTER_BOUND('',#1161,.T.);
#793=FACE_OUTER_BOUND('',#1162,.T.);
#794=FACE_OUTER_BOUND('',#1163,.T.);
#795=FACE_OUTER_BOUND('',#1164,.T.);
#796=FACE_OUTER_BOUND('',#1165,.T.);
#797=FACE_OUTER_BOUND('',#1166,.T.);
#798=FACE_OUTER_BOUND('',#1167,.T.);
#799=FACE_OUTER_BOUND('',#1168,.T.);
#800=FACE_OUTER_BOUND('',#1169,.T.);
#801=FACE_OUTER_BOUND('',#1170,.T.);
#802=FACE_OUTER_BOUND('',#1171,.T.);
#803=FACE_OUTER_BOUND('',#1173,.T.);
#804=FACE_OUTER_BOUND('',#1174,.T.);
#1158=EDGE_LOOP('',(#3719,#3720,#3721,#3722));
#1159=EDGE_LOOP('',(#3723,#3724,#3725,#3726));
#1160=EDGE_LOOP('',(#3727,#3728,#3729,#3730));
#1161=EDGE_LOOP('',(#3731,#3732,#3733,#3734));
#1162=EDGE_LOOP('',(#3735,#3736,#3737,#3738));
#1163=EDGE_LOOP('',(#3739,#3740,#3741,#3742));
#1164=EDGE_LOOP('',(#3743,#3744,#3745,#3746,#3747,#3748));
#1165=EDGE_LOOP('',(#3749,#3750,#3751,#3752,#3753,#3754));
#1166=EDGE_LOOP('',(#3755));
#1167=EDGE_LOOP('',(#3756));
#1168=EDGE_LOOP('',(#3757,#3758,#3759,#3760));
#1169=EDGE_LOOP('',(#3761,#3762,#3763,#3764));
#1170=EDGE_LOOP('',(#3765,#3766,#3767,#3768));
#1171=EDGE_LOOP('',(#3769));
#1172=EDGE_LOOP('',(#3770));
#1173=EDGE_LOOP('',(#3771,#3772,#3773,#3774));
#1174=EDGE_LOOP('',(#3775,#3776,#3777,#3778));
#1462=LINE('',#9858,#1714);
#1463=LINE('',#9860,#1715);
#1464=LINE('',#9862,#1716);
#1465=LINE('',#9863,#1717);
#1466=LINE('',#9866,#1718);
#1467=LINE('',#9868,#1719);
#1468=LINE('',#9869,#1720);
#1469=LINE('',#9872,#1721);
#1470=LINE('',#9874,#1722);
#1471=LINE('',#9875,#1723);
#1472=LINE('',#9878,#1724);
#1473=LINE('',#9880,#1725);
#1474=LINE('',#9881,#1726);
#1475=LINE('',#9884,#1727);
#1476=LINE('',#9886,#1728);
#1477=LINE('',#9887,#1729);
#1478=LINE('',#9889,#1730);
#1479=LINE('',#9890,#1731);
#1480=LINE('',#9902,#1732);
#1481=LINE('',#9906,#1733);
#1482=LINE('',#9910,#1734);
#1483=LINE('',#9917,#1735);
#1484=LINE('',#9919,#1736);
#1714=VECTOR('',#6381,1.);
#1715=VECTOR('',#6382,1.);
#1716=VECTOR('',#6383,1.);
#1717=VECTOR('',#6384,1.);
#1718=VECTOR('',#6387,1.);
#1719=VECTOR('',#6388,1.);
#1720=VECTOR('',#6389,1.);
#1721=VECTOR('',#6392,1.);
#1722=VECTOR('',#6393,1.);
#1723=VECTOR('',#6394,1.);
#1724=VECTOR('',#6397,1.);
#1725=VECTOR('',#6398,1.);
#1726=VECTOR('',#6399,1.);
#1727=VECTOR('',#6402,1.);
#1728=VECTOR('',#6403,1.);
#1729=VECTOR('',#6404,1.);
#1730=VECTOR('',#6407,1.);
#1731=VECTOR('',#6408,1.);
#1732=VECTOR('',#6425,0.4);
#1733=VECTOR('',#6430,0.425);
#1734=VECTOR('',#6435,0.41);
#1735=VECTOR('',#6444,0.26);
#1736=VECTOR('',#6447,0.25);
#1999=CIRCLE('',#5321,0.24505);
#2000=CIRCLE('',#5323,0.375);
#2001=CIRCLE('',#5325,0.425);
#2002=CIRCLE('',#5327,0.425);
#2003=CIRCLE('',#5329,0.395);
#2004=CIRCLE('',#5331,0.27);
#2005=CIRCLE('',#5333,0.24505);
#2338=VERTEX_POINT('',#9856);
#2339=VERTEX_POINT('',#9857);
#2340=VERTEX_POINT('',#9859);
#2341=VERTEX_POINT('',#9861);
#2342=VERTEX_POINT('',#9865);
#2343=VERTEX_POINT('',#9867);
#2344=VERTEX_POINT('',#9871);
#2345=VERTEX_POINT('',#9873);
#2346=VERTEX_POINT('',#9877);
#2347=VERTEX_POINT('',#9879);
#2348=VERTEX_POINT('',#9883);
#2349=VERTEX_POINT('',#9885);
#2350=VERTEX_POINT('',#9894);
#2351=VERTEX_POINT('',#9897);
#2352=VERTEX_POINT('',#9900);
#2353=VERTEX_POINT('',#9904);
#2354=VERTEX_POINT('',#9908);
#2355=VERTEX_POINT('',#9912);
#2356=VERTEX_POINT('',#9915);
#2836=EDGE_CURVE('',#2338,#2339,#1462,.T.);
#2837=EDGE_CURVE('',#2339,#2340,#1463,.T.);
#2838=EDGE_CURVE('',#2340,#2341,#1464,.T.);
#2839=EDGE_CURVE('',#2338,#2341,#1465,.T.);
#2840=EDGE_CURVE('',#2339,#2342,#1466,.T.);
#2841=EDGE_CURVE('',#2342,#2343,#1467,.T.);
#2842=EDGE_CURVE('',#2343,#2340,#1468,.T.);
#2843=EDGE_CURVE('',#2342,#2344,#1469,.T.);
#2844=EDGE_CURVE('',#2344,#2345,#1470,.T.);
#2845=EDGE_CURVE('',#2345,#2343,#1471,.T.);
#2846=EDGE_CURVE('',#2344,#2346,#1472,.T.);
#2847=EDGE_CURVE('',#2346,#2347,#1473,.T.);
#2848=EDGE_CURVE('',#2347,#2345,#1474,.T.);
#2849=EDGE_CURVE('',#2346,#2348,#1475,.T.);
#2850=EDGE_CURVE('',#2348,#2349,#1476,.T.);
#2851=EDGE_CURVE('',#2349,#2347,#1477,.T.);
#2852=EDGE_CURVE('',#2348,#2338,#1478,.T.);
#2853=EDGE_CURVE('',#2341,#2349,#1479,.T.);
#2854=EDGE_CURVE('',#2350,#2350,#1999,.T.);
#2855=EDGE_CURVE('',#2351,#2351,#2000,.T.);
#2856=EDGE_CURVE('',#2352,#2352,#2001,.T.);
#2857=EDGE_CURVE('',#2352,#2351,#1480,.T.);
#2858=EDGE_CURVE('',#2353,#2353,#2002,.T.);
#2859=EDGE_CURVE('',#2353,#2352,#1481,.T.);
#2860=EDGE_CURVE('',#2354,#2354,#2003,.T.);
#2861=EDGE_CURVE('',#2354,#2353,#1482,.T.);
#2862=EDGE_CURVE('',#2355,#2355,#2004,.T.);
#2863=EDGE_CURVE('',#2356,#2356,#2005,.F.);
#2864=EDGE_CURVE('',#2356,#2355,#1483,.T.);
#2865=EDGE_CURVE('',#2350,#2356,#1484,.T.);
#3719=ORIENTED_EDGE('',*,*,#2836,.T.);
#3720=ORIENTED_EDGE('',*,*,#2837,.T.);
#3721=ORIENTED_EDGE('',*,*,#2838,.T.);
#3722=ORIENTED_EDGE('',*,*,#2839,.F.);
#3723=ORIENTED_EDGE('',*,*,#2840,.T.);
#3724=ORIENTED_EDGE('',*,*,#2841,.T.);
#3725=ORIENTED_EDGE('',*,*,#2842,.T.);
#3726=ORIENTED_EDGE('',*,*,#2837,.F.);
#3727=ORIENTED_EDGE('',*,*,#2843,.T.);
#3728=ORIENTED_EDGE('',*,*,#2844,.T.);
#3729=ORIENTED_EDGE('',*,*,#2845,.T.);
#3730=ORIENTED_EDGE('',*,*,#2841,.F.);
#3731=ORIENTED_EDGE('',*,*,#2846,.T.);
#3732=ORIENTED_EDGE('',*,*,#2847,.T.);
#3733=ORIENTED_EDGE('',*,*,#2848,.T.);
#3734=ORIENTED_EDGE('',*,*,#2844,.F.);
#3735=ORIENTED_EDGE('',*,*,#2849,.T.);
#3736=ORIENTED_EDGE('',*,*,#2850,.T.);
#3737=ORIENTED_EDGE('',*,*,#2851,.T.);
#3738=ORIENTED_EDGE('',*,*,#2847,.F.);
#3739=ORIENTED_EDGE('',*,*,#2852,.T.);
#3740=ORIENTED_EDGE('',*,*,#2839,.T.);
#3741=ORIENTED_EDGE('',*,*,#2853,.T.);
#3742=ORIENTED_EDGE('',*,*,#2850,.F.);
#3743=ORIENTED_EDGE('',*,*,#2852,.F.);
#3744=ORIENTED_EDGE('',*,*,#2849,.F.);
#3745=ORIENTED_EDGE('',*,*,#2846,.F.);
#3746=ORIENTED_EDGE('',*,*,#2843,.F.);
#3747=ORIENTED_EDGE('',*,*,#2840,.F.);
#3748=ORIENTED_EDGE('',*,*,#2836,.F.);
#3749=ORIENTED_EDGE('',*,*,#2853,.F.);
#3750=ORIENTED_EDGE('',*,*,#2838,.F.);
#3751=ORIENTED_EDGE('',*,*,#2842,.F.);
#3752=ORIENTED_EDGE('',*,*,#2845,.F.);
#3753=ORIENTED_EDGE('',*,*,#2848,.F.);
#3754=ORIENTED_EDGE('',*,*,#2851,.F.);
#3755=ORIENTED_EDGE('',*,*,#2854,.F.);
#3756=ORIENTED_EDGE('',*,*,#2855,.F.);
#3757=ORIENTED_EDGE('',*,*,#2856,.F.);
#3758=ORIENTED_EDGE('',*,*,#2857,.T.);
#3759=ORIENTED_EDGE('',*,*,#2855,.T.);
#3760=ORIENTED_EDGE('',*,*,#2857,.F.);
#3761=ORIENTED_EDGE('',*,*,#2858,.F.);
#3762=ORIENTED_EDGE('',*,*,#2859,.T.);
#3763=ORIENTED_EDGE('',*,*,#2856,.T.);
#3764=ORIENTED_EDGE('',*,*,#2859,.F.);
#3765=ORIENTED_EDGE('',*,*,#2860,.F.);
#3766=ORIENTED_EDGE('',*,*,#2861,.T.);
#3767=ORIENTED_EDGE('',*,*,#2858,.T.);
#3768=ORIENTED_EDGE('',*,*,#2861,.F.);
#3769=ORIENTED_EDGE('',*,*,#2860,.T.);
#3770=ORIENTED_EDGE('',*,*,#2862,.F.);
#3771=ORIENTED_EDGE('',*,*,#2863,.F.);
#3772=ORIENTED_EDGE('',*,*,#2864,.T.);
#3773=ORIENTED_EDGE('',*,*,#2862,.T.);
#3774=ORIENTED_EDGE('',*,*,#2864,.F.);
#3775=ORIENTED_EDGE('',*,*,#2854,.T.);
#3776=ORIENTED_EDGE('',*,*,#2865,.T.);
#3777=ORIENTED_EDGE('',*,*,#2863,.T.);
#3778=ORIENTED_EDGE('',*,*,#2865,.F.);
#4382=CYLINDRICAL_SURFACE('',#5326,0.425);
#4383=CYLINDRICAL_SURFACE('',#5334,0.24505);
#4554=ADVANCED_FACE('',(#789),#579,.F.);
#4555=ADVANCED_FACE('',(#790),#580,.F.);
#4556=ADVANCED_FACE('',(#791),#581,.F.);
#4557=ADVANCED_FACE('',(#792),#582,.F.);
#4558=ADVANCED_FACE('',(#793),#583,.F.);
#4559=ADVANCED_FACE('',(#794),#584,.F.);
#4560=ADVANCED_FACE('',(#795),#585,.F.);
#4561=ADVANCED_FACE('',(#796),#586,.F.);
#4562=ADVANCED_FACE('',(#797),#587,.F.);
#4563=ADVANCED_FACE('',(#798),#588,.T.);
#4564=ADVANCED_FACE('',(#799),#29,.T.);
#4565=ADVANCED_FACE('',(#800),#4382,.T.);
#4566=ADVANCED_FACE('',(#801),#30,.T.);
#4567=ADVANCED_FACE('',(#802,#489),#589,.T.);
#4568=ADVANCED_FACE('',(#803),#31,.T.);
#4569=ADVANCED_FACE('',(#804),#4383,.T.);
#4714=CLOSED_SHELL('',(#4554,#4555,#4556,#4557,#4558,#4559,#4560,#4561));
#4715=CLOSED_SHELL('',(#4562,#4563,#4564,#4565,#4566,#4567,#4568,#4569));
#5311=AXIS2_PLACEMENT_3D('',#9854,#6377,#6378);
#5312=AXIS2_PLACEMENT_3D('',#9855,#6379,#6380);
#5313=AXIS2_PLACEMENT_3D('',#9864,#6385,#6386);
#5314=AXIS2_PLACEMENT_3D('',#9870,#6390,#6391);
#5315=AXIS2_PLACEMENT_3D('',#9876,#6395,#6396);
#5316=AXIS2_PLACEMENT_3D('',#9882,#6400,#6401);
#5317=AXIS2_PLACEMENT_3D('',#9888,#6405,#6406);
#5318=AXIS2_PLACEMENT_3D('',#9891,#6409,#6410);
#5319=AXIS2_PLACEMENT_3D('',#9892,#6411,#6412);
#5320=AXIS2_PLACEMENT_3D('',#9893,#6413,#6414);
#5321=AXIS2_PLACEMENT_3D('',#9895,#6415,#6416);
#5322=AXIS2_PLACEMENT_3D('',#9896,#6417,#6418);
#5323=AXIS2_PLACEMENT_3D('',#9898,#6419,#6420);
#5324=AXIS2_PLACEMENT_3D('',#9899,#6421,#6422);
#5325=AXIS2_PLACEMENT_3D('',#9901,#6423,#6424);
#5326=AXIS2_PLACEMENT_3D('',#9903,#6426,#6427);
#5327=AXIS2_PLACEMENT_3D('',#9905,#6428,#6429);
#5328=AXIS2_PLACEMENT_3D('',#9907,#6431,#6432);
#5329=AXIS2_PLACEMENT_3D('',#9909,#6433,#6434);
#5330=AXIS2_PLACEMENT_3D('',#9911,#6436,#6437);
#5331=AXIS2_PLACEMENT_3D('',#9913,#6438,#6439);
#5332=AXIS2_PLACEMENT_3D('',#9914,#6440,#6441);
#5333=AXIS2_PLACEMENT_3D('',#9916,#6442,#6443);
#5334=AXIS2_PLACEMENT_3D('',#9918,#6445,#6446);
#6377=DIRECTION('axis',(0.,0.,1.));
#6378=DIRECTION('refdir',(1.,0.,0.));
#6379=DIRECTION('center_axis',(0.866025403784439,0.,-0.5));
#6380=DIRECTION('ref_axis',(0.5,0.,0.866025403784439));
#6381=DIRECTION('',(-0.5,0.,-0.866025403784439));
#6382=DIRECTION('',(0.,-1.,0.));
#6383=DIRECTION('',(0.5,0.,0.866025403784439));
#6384=DIRECTION('',(0.,-1.,0.));
#6385=DIRECTION('center_axis',(1.20185167898973E-16,0.,-1.));
#6386=DIRECTION('ref_axis',(1.,0.,1.20185167898973E-16));
#6387=DIRECTION('',(-1.,0.,-1.20185167898973E-16));
#6388=DIRECTION('',(0.,-1.,0.));
#6389=DIRECTION('',(1.,0.,1.20185167898973E-16));
#6390=DIRECTION('center_axis',(-0.866025403784439,0.,-0.5));
#6391=DIRECTION('ref_axis',(0.5,0.,-0.866025403784439));
#6392=DIRECTION('',(-0.5,0.,0.866025403784439));
#6393=DIRECTION('',(0.,-1.,0.));
#6394=DIRECTION('',(0.5,0.,-0.866025403784439));
#6395=DIRECTION('center_axis',(-0.866025403784439,0.,0.5));
#6396=DIRECTION('ref_axis',(-0.5,0.,-0.866025403784439));
#6397=DIRECTION('',(0.5,0.,0.866025403784439));
#6398=DIRECTION('',(0.,-1.,0.));
#6399=DIRECTION('',(-0.5,0.,-0.866025403784439));
#6400=DIRECTION('center_axis',(-2.40370335797945E-16,0.,1.));
#6401=DIRECTION('ref_axis',(-1.,0.,-2.40370335797945E-16));
#6402=DIRECTION('',(1.,0.,2.40370335797945E-16));
#6403=DIRECTION('',(0.,-1.,0.));
#6404=DIRECTION('',(-1.,0.,-2.40370335797945E-16));
#6405=DIRECTION('center_axis',(0.866025403784439,0.,0.5));
#6406=DIRECTION('ref_axis',(-0.5,0.,0.866025403784439));
#6407=DIRECTION('',(0.5,0.,-0.866025403784439));
#6408=DIRECTION('',(-0.5,0.,0.866025403784439));
#6409=DIRECTION('center_axis',(0.,1.,0.));
#6410=DIRECTION('ref_axis',(1.,0.,0.));
#6411=DIRECTION('center_axis',(0.,-1.,0.));
#6412=DIRECTION('ref_axis',(0.,0.,-1.));
#6413=DIRECTION('center_axis',(0.,1.,0.));
#6414=DIRECTION('ref_axis',(1.,0.,0.));
#6415=DIRECTION('center_axis',(0.,1.,0.));
#6416=DIRECTION('ref_axis',(1.,0.,0.));
#6417=DIRECTION('center_axis',(0.,1.,0.));
#6418=DIRECTION('ref_axis',(0.,0.,1.));
#6419=DIRECTION('center_axis',(0.,-1.,0.));
#6420=DIRECTION('ref_axis',(1.,0.,0.));
#6421=DIRECTION('center_axis',(0.,-1.,0.));
#6422=DIRECTION('ref_axis',(1.,0.,0.));
#6423=DIRECTION('center_axis',(0.,-1.,0.));
#6424=DIRECTION('ref_axis',(1.,0.,0.));
#6425=DIRECTION('',(0.707106781186548,0.707106781186547,8.65956056235493E-17));
#6426=DIRECTION('center_axis',(0.,-1.,0.));
#6427=DIRECTION('ref_axis',(1.,0.,0.));
#6428=DIRECTION('center_axis',(0.,-1.,0.));
#6429=DIRECTION('ref_axis',(1.,0.,0.));
#6430=DIRECTION('',(0.,1.,0.));
#6431=DIRECTION('center_axis',(0.,1.,0.));
#6432=DIRECTION('ref_axis',(1.,0.,0.));
#6433=DIRECTION('center_axis',(0.,-1.,0.));
#6434=DIRECTION('ref_axis',(1.,0.,0.));
#6435=DIRECTION('',(-0.707106781186547,0.707106781186548,-8.65956056235493E-17));
#6436=DIRECTION('center_axis',(0.,-1.,0.));
#6437=DIRECTION('ref_axis',(0.,0.,-1.));
#6438=DIRECTION('center_axis',(0.,-1.,0.));
#6439=DIRECTION('ref_axis',(1.,0.,0.));
#6440=DIRECTION('center_axis',(0.,1.,0.));
#6441=DIRECTION('ref_axis',(1.,0.,0.));
#6442=DIRECTION('center_axis',(0.,1.,0.));
#6443=DIRECTION('ref_axis',(1.,0.,0.));
#6444=DIRECTION('',(-0.447213595499958,0.894427190999916,-5.47678698264203E-17));
#6445=DIRECTION('center_axis',(0.,-1.,0.));
#6446=DIRECTION('ref_axis',(1.,0.,0.));
#6447=DIRECTION('',(0.,1.,0.));
#9854=CARTESIAN_POINT('',(0.,0.,0.));
#9855=CARTESIAN_POINT('Origin',(0.115470053837925,-0.5,-0.2));
#9856=CARTESIAN_POINT('',(0.23094010767585,-0.5,0.));
#9857=CARTESIAN_POINT('',(0.115470053837925,-0.5,-0.2));
#9858=CARTESIAN_POINT('',(0.23094010767585,-0.5,0.));
#9859=CARTESIAN_POINT('',(0.115470053837925,-0.8,-0.2));
#9860=CARTESIAN_POINT('',(0.115470053837925,-0.5,-0.2));
#9861=CARTESIAN_POINT('',(0.23094010767585,-0.8,0.));
#9862=CARTESIAN_POINT('',(0.23094010767585,-0.8,0.));
#9863=CARTESIAN_POINT('',(0.23094010767585,-0.5,0.));
#9864=CARTESIAN_POINT('Origin',(-0.115470053837925,-0.5,-0.2));
#9865=CARTESIAN_POINT('',(-0.115470053837925,-0.5,-0.2));
#9866=CARTESIAN_POINT('',(0.115470053837925,-0.5,-0.2));
#9867=CARTESIAN_POINT('',(-0.115470053837925,-0.8,-0.2));
#9868=CARTESIAN_POINT('',(-0.115470053837925,-0.5,-0.2));
#9869=CARTESIAN_POINT('',(0.115470053837925,-0.8,-0.2));
#9870=CARTESIAN_POINT('Origin',(-0.23094010767585,-0.5,-2.77555756156289E-17));
#9871=CARTESIAN_POINT('',(-0.23094010767585,-0.5,-2.82820063659975E-17));
#9872=CARTESIAN_POINT('',(-0.115470053837925,-0.5,-0.2));
#9873=CARTESIAN_POINT('',(-0.23094010767585,-0.8,-2.77555756156289E-17));
#9874=CARTESIAN_POINT('',(-0.23094010767585,-0.5,-2.82820063659975E-17));
#9875=CARTESIAN_POINT('',(-0.115470053837925,-0.8,-0.2));
#9876=CARTESIAN_POINT('Origin',(-0.115470053837925,-0.5,0.2));
#9877=CARTESIAN_POINT('',(-0.115470053837925,-0.5,0.2));
#9878=CARTESIAN_POINT('',(-0.23094010767585,-0.5,-2.82820063659975E-17));
#9879=CARTESIAN_POINT('',(-0.115470053837925,-0.8,0.2));
#9880=CARTESIAN_POINT('',(-0.115470053837925,-0.5,0.2));
#9881=CARTESIAN_POINT('',(-0.23094010767585,-0.8,-2.82820063659975E-17));
#9882=CARTESIAN_POINT('Origin',(0.115470053837925,-0.5,0.2));
#9883=CARTESIAN_POINT('',(0.115470053837925,-0.5,0.2));
#9884=CARTESIAN_POINT('',(-0.115470053837925,-0.5,0.2));
#9885=CARTESIAN_POINT('',(0.115470053837925,-0.8,0.2));
#9886=CARTESIAN_POINT('',(0.115470053837925,-0.5,0.2));
#9887=CARTESIAN_POINT('',(-0.115470053837925,-0.8,0.2));
#9888=CARTESIAN_POINT('Origin',(0.23094010767585,-0.5,0.));
#9889=CARTESIAN_POINT('',(0.115470053837925,-0.5,0.2));
#9890=CARTESIAN_POINT('',(0.115470053837925,-0.8,0.2));
#9891=CARTESIAN_POINT('Origin',(0.,-0.5,0.));
#9892=CARTESIAN_POINT('Origin',(0.,-0.8,0.));
#9893=CARTESIAN_POINT('Origin',(0.,-1.4,0.));
#9894=CARTESIAN_POINT('',(-0.24505,-1.4,3.00099698131059E-17));
#9895=CARTESIAN_POINT('Origin',(0.,-1.4,0.));
#9896=CARTESIAN_POINT('Origin',(0.375,0.5,0.));
#9897=CARTESIAN_POINT('',(-0.375,0.5,-4.59242549680257E-17));
#9898=CARTESIAN_POINT('Origin',(0.,0.5,0.));
#9899=CARTESIAN_POINT('Origin',(0.,0.475,0.));
#9900=CARTESIAN_POINT('',(-0.425,0.45,-5.20474889637625E-17));
#9901=CARTESIAN_POINT('Origin',(0.,0.45,0.));
#9902=CARTESIAN_POINT('',(-0.4,0.475,-4.89858719658941E-17));
#9903=CARTESIAN_POINT('Origin',(0.,0.24,0.));
#9904=CARTESIAN_POINT('',(-0.425,0.0299999999999998,-5.20474889637625E-17));
#9905=CARTESIAN_POINT('Origin',(0.,0.0299999999999998,0.));
#9906=CARTESIAN_POINT('',(-0.425,0.24,-5.20474889637625E-17));
#9907=CARTESIAN_POINT('Origin',(0.,0.0150000000000001,0.));
#9908=CARTESIAN_POINT('',(-0.395,4.85722573273506E-17,-4.83735485663204E-17));
#9909=CARTESIAN_POINT('Origin',(0.,0.,0.));
#9910=CARTESIAN_POINT('',(-0.41,0.0150000000000001,-5.02105187650415E-17));
#9911=CARTESIAN_POINT('Origin',(0.27,0.,0.));
#9912=CARTESIAN_POINT('',(-0.27,0.,-3.30654635769785E-17));
#9913=CARTESIAN_POINT('Origin',(0.,0.,0.));
#9914=CARTESIAN_POINT('Origin',(0.,-0.02,0.));
#9915=CARTESIAN_POINT('',(-0.24505,-0.0498999999999999,3.00099698131059E-17));
#9916=CARTESIAN_POINT('Origin',(0.,-0.0498999999999999,0.));
#9917=CARTESIAN_POINT('',(-0.26,-0.02,-3.18408167778312E-17));
#9918=CARTESIAN_POINT('Origin',(0.,-0.995,0.));
#9919=CARTESIAN_POINT('',(-0.24505,-0.995,-3.00099698131059E-17));
#10982=UNCERTAINTY_MEASURE_WITH_UNIT(LENGTH_MEASURE(0.001),#11036,
'DISTANCE_ACCURACY_VALUE',
'Maximum model space distance between geometric entities at asserted c
onnectivities');
#11002=UNCERTAINTY_MEASURE_WITH_UNIT(LENGTH_MEASURE(0.001),#11036,
'DISTANCE_ACCURACY_VALUE',
'Maximum model space distance between geometric entities at asserted c
onnectivities');
#11015=(
GEOMETRIC_REPRESENTATION_CONTEXT(3)
GLOBAL_UNCERTAINTY_ASSIGNED_CONTEXT((#10982))
GLOBAL_UNIT_ASSIGNED_CONTEXT((#11036,#11038,#11039))
REPRESENTATION_CONTEXT('','3D')
);
#11035=(
GEOMETRIC_REPRESENTATION_CONTEXT(3)
GLOBAL_UNCERTAINTY_ASSIGNED_CONTEXT((#11002))
GLOBAL_UNIT_ASSIGNED_CONTEXT((#11036,#11038,#11039))
REPRESENTATION_CONTEXT('','3D')
);
#11036=(
LENGTH_UNIT()
NAMED_UNIT(*)
SI_UNIT(.CENTI.,.METRE.)
);
#11038=(
NAMED_UNIT(*)
PLANE_ANGLE_UNIT()
SI_UNIT($,.RADIAN.)
);
#11039=(
NAMED_UNIT(*)
SI_UNIT($,.STERADIAN.)
SOLID_ANGLE_UNIT()
);
#11052=SHAPE_DEFINITION_REPRESENTATION(#11086,#11165);
#11086=PRODUCT_DEFINITION_SHAPE('',$,#11198);
#11165=SHAPE_REPRESENTATION('',(#5311),#11015);
#11185=PRODUCT_DEFINITION_CONTEXT('part definition',#11283,'design');
#11198=PRODUCT_DEFINITION('M5x14 Cap Screw','M5x14 Cap Screw',#11230,#11185);
#11230=PRODUCT_DEFINITION_FORMATION('',$,#11297);
#11283=APPLICATION_CONTEXT(
'Core Data for Automotive Mechanical Design Process');
#11284=PRODUCT_CONTEXT('part definition',#11283,'mechanical');
#11297=PRODUCT('M5x14 Cap Screw','M5x14 Cap Screw','M5x14 Cap Screw',(#11284));
#11387=COLOUR_RGB('Black',0.12,0.14,0.17);
#11388=FILL_AREA_STYLE_COLOUR('',#11387);
#11389=FILL_AREA_STYLE('',(#11388));
#11390=SURFACE_STYLE_FILL_AREA(#11389);
#11391=SURFACE_SIDE_STYLE('',(#11390));
#11392=SURFACE_STYLE_USAGE(.BOTH.,#11391);
#11393=PRESENTATION_STYLE_ASSIGNMENT((#11392));
ENDSEC;
END-ISO-10303-21;
